ISO-10303-21;
HEADER;
/* Generated by software containing ST-Developer
 * from STEP Tools, Inc. (www.steptools.com) 
 */

FILE_DESCRIPTION(
/* description */ ('Independent two-stage fixed-ring planetary gearbox,24/24/72 teeth,mod
ule2,20deg involutes,three planets per stage,4:1 x4:1=16:1. Native cut
-space/fillet/pattern tooth profiles derived from reusable gear blanks
; shared sun/planet/ring/carrier parts across both stages. Captured br
onze-journal input/carriers, headed retained planet pins, keyed inters
tage drive and modular keyed output interface. Native ideal gear links
; no torque, precision grade, production backlash/fits, lubrication, s
peed or life rating.'),
/* implementation_level */ '2;1');

FILE_NAME(
/* name */ 'Journal thrust washer.step',
/* time_stamp */ '2026-11-08T19:10:00-08:00',
/* author */ (''),
/* organization */ (''),
/* preprocessor_version */ 'ST-DEVELOPER v20.2',
/* originating_system */ 'Autodesk Translation Framework v15.17.0.0',
/* authorisation */ '');

FILE_SCHEMA (('AUTOMOTIVE_DESIGN { 1 0 10303 214 3 1 1 }'));
ENDSEC;

DATA;
#10=MECHANICAL_DESIGN_GEOMETRIC_PRESENTATION_REPRESENTATION('',(#1178),#259224);
#1138=SHAPE_REPRESENTATION_RELATIONSHIP('SRR','None',#259385,#1158);
#1158=ADVANCED_BREP_SHAPE_REPRESENTATION('',(#1198),#259219);
#1178=STYLED_ITEM('',(#259485),#1198);
#1198=MANIFOLD_SOLID_BREP('Body1',#25165);
#1314=FACE_BOUND('',#4430,.T.);
#1315=FACE_BOUND('',#4432,.T.);
#1676=PLANE('',#27146);
#1677=PLANE('',#27147);
#2970=FACE_OUTER_BOUND('',#4427,.T.);
#2971=FACE_OUTER_BOUND('',#4428,.T.);
#2972=FACE_OUTER_BOUND('',#4429,.T.);
#2973=FACE_OUTER_BOUND('',#4431,.T.);
#4427=EDGE_LOOP('',(#22706,#22707,#22708,#22709));
#4428=EDGE_LOOP('',(#22710,#22711,#22712,#22713));
#4429=EDGE_LOOP('',(#22714));
#4430=EDGE_LOOP('',(#22715));
#4431=EDGE_LOOP('',(#22716));
#4432=EDGE_LOOP('',(#22717));
#5365=CIRCLE('',#27141,16.);
#5366=CIRCLE('',#27142,16.);
#5367=CIRCLE('',#27144,20.);
#5368=CIRCLE('',#27145,20.);
#7774=LINE('',#256035,#8959);
#7775=LINE('',#256041,#8960);
#8959=VECTOR('',#31943,16.);
#8960=VECTOR('',#31950,20.);
#11473=VERTEX_POINT('',#256032);
#11474=VERTEX_POINT('',#256034);
#11475=VERTEX_POINT('',#256038);
#11476=VERTEX_POINT('',#256040);
#15238=EDGE_CURVE('',#11473,#11473,#5365,.T.);
#15239=EDGE_CURVE('',#11473,#11474,#7774,.T.);
#15240=EDGE_CURVE('',#11474,#11474,#5366,.T.);
#15241=EDGE_CURVE('',#11475,#11475,#5367,.T.);
#15242=EDGE_CURVE('',#11475,#11476,#7775,.T.);
#15243=EDGE_CURVE('',#11476,#11476,#5368,.T.);
#22706=ORIENTED_EDGE('',*,*,#15238,.F.);
#22707=ORIENTED_EDGE('',*,*,#15239,.T.);
#22708=ORIENTED_EDGE('',*,*,#15240,.T.);
#22709=ORIENTED_EDGE('',*,*,#15239,.F.);
#22710=ORIENTED_EDGE('',*,*,#15241,.F.);
#22711=ORIENTED_EDGE('',*,*,#15242,.T.);
#22712=ORIENTED_EDGE('',*,*,#15243,.T.);
#22713=ORIENTED_EDGE('',*,*,#15242,.F.);
#22714=ORIENTED_EDGE('',*,*,#15241,.T.);
#22715=ORIENTED_EDGE('',*,*,#15238,.T.);
#22716=ORIENTED_EDGE('',*,*,#15243,.F.);
#22717=ORIENTED_EDGE('',*,*,#15240,.F.);
#23754=CYLINDRICAL_SURFACE('',#27140,16.);
#23755=CYLINDRICAL_SURFACE('',#27143,20.);
#25076=ADVANCED_FACE('',(#2970),#23754,.F.);
#25077=ADVANCED_FACE('',(#2971),#23755,.T.);
#25078=ADVANCED_FACE('',(#2972,#1314),#1676,.T.);
#25079=ADVANCED_FACE('',(#2973,#1315),#1677,.F.);
#25165=CLOSED_SHELL('',(#25076,#25077,#25078,#25079));
#27139=AXIS2_PLACEMENT_3D('',#256030,#31937,#31938);
#27140=AXIS2_PLACEMENT_3D('',#256031,#31939,#31940);
#27141=AXIS2_PLACEMENT_3D('',#256033,#31941,#31942);
#27142=AXIS2_PLACEMENT_3D('',#256036,#31944,#31945);
#27143=AXIS2_PLACEMENT_3D('',#256037,#31946,#31947);
#27144=AXIS2_PLACEMENT_3D('',#256039,#31948,#31949);
#27145=AXIS2_PLACEMENT_3D('',#256042,#31951,#31952);
#27146=AXIS2_PLACEMENT_3D('',#256043,#31953,#31954);
#27147=AXIS2_PLACEMENT_3D('',#256044,#31955,#31956);
#31937=DIRECTION('axis',(0.,0.,1.));
#31938=DIRECTION('refdir',(1.,0.,0.));
#31939=DIRECTION('center_axis',(0.,0.,1.));
#31940=DIRECTION('ref_axis',(1.,0.,0.));
#31941=DIRECTION('center_axis',(0.,0.,-1.));
#31942=DIRECTION('ref_axis',(1.,0.,0.));
#31943=DIRECTION('',(0.,0.,-1.));
#31944=DIRECTION('center_axis',(0.,0.,-1.));
#31945=DIRECTION('ref_axis',(1.,0.,0.));
#31946=DIRECTION('center_axis',(0.,0.,1.));
#31947=DIRECTION('ref_axis',(1.,0.,0.));
#31948=DIRECTION('center_axis',(0.,0.,1.));
#31949=DIRECTION('ref_axis',(1.,0.,0.));
#31950=DIRECTION('',(0.,0.,-1.));
#31951=DIRECTION('center_axis',(0.,0.,1.));
#31952=DIRECTION('ref_axis',(1.,0.,0.));
#31953=DIRECTION('center_axis',(0.,0.,1.));
#31954=DIRECTION('ref_axis',(1.,0.,0.));
#31955=DIRECTION('center_axis',(0.,0.,1.));
#31956=DIRECTION('ref_axis',(1.,0.,0.));
#256030=CARTESIAN_POINT('',(0.,0.,0.));
#256031=CARTESIAN_POINT('Origin',(0.,0.,0.));
#256032=CARTESIAN_POINT('',(-16.,-1.95943487863577E-15,2.));
#256033=CARTESIAN_POINT('Origin',(0.,0.,2.));
#256034=CARTESIAN_POINT('',(-16.,-1.95943487863577E-15,0.));
#256035=CARTESIAN_POINT('',(-16.,-1.95943487863577E-15,0.));
#256036=CARTESIAN_POINT('Origin',(0.,0.,0.));
#256037=CARTESIAN_POINT('Origin',(0.,0.,0.));
#256038=CARTESIAN_POINT('',(-20.,-2.44929359829471E-15,2.));
#256039=CARTESIAN_POINT('Origin',(0.,0.,2.));
#256040=CARTESIAN_POINT('',(-20.,-2.44929359829471E-15,0.));
#256041=CARTESIAN_POINT('',(-20.,-2.44929359829471E-15,0.));
#256042=CARTESIAN_POINT('Origin',(0.,0.,0.));
#256043=CARTESIAN_POINT('Origin',(0.,0.,2.));
#256044=CARTESIAN_POINT('Origin',(0.,0.,0.));
#259197=UNCERTAINTY_MEASURE_WITH_UNIT(LENGTH_MEASURE(0.01),#259225,
'DISTANCE_ACCURACY_VALUE',
'Maximum model space distance between geometric entities at asserted c
onnectivities');
#259202=UNCERTAINTY_MEASURE_WITH_UNIT(LENGTH_MEASURE(0.01),#259225,
'DISTANCE_ACCURACY_VALUE',
'Maximum model space distance between geometric entities at asserted c
onnectivities');
#259219=(
GEOMETRIC_REPRESENTATION_CONTEXT(3)
GLOBAL_UNCERTAINTY_ASSIGNED_CONTEXT((#259197))
GLOBAL_UNIT_ASSIGNED_CONTEXT((#259225,#259227,#259228))
REPRESENTATION_CONTEXT('','3D')
);
#259224=(
GEOMETRIC_REPRESENTATION_CONTEXT(3)
GLOBAL_UNCERTAINTY_ASSIGNED_CONTEXT((#259202))
GLOBAL_UNIT_ASSIGNED_CONTEXT((#259225,#259227,#259228))
REPRESENTATION_CONTEXT('','3D')
);
#259225=(
LENGTH_UNIT()
NAMED_UNIT(*)
SI_UNIT(.MILLI.,.METRE.)
);
#259227=(
NAMED_UNIT(*)
PLANE_ANGLE_UNIT()
SI_UNIT($,.RADIAN.)
);
#259228=(
NAMED_UNIT(*)
SI_UNIT($,.STERADIAN.)
SOLID_ANGLE_UNIT()
);
#259245=SHAPE_DEFINITION_REPRESENTATION(#259266,#259385);
#259266=PRODUCT_DEFINITION_SHAPE('',$,#259407);
#259385=SHAPE_REPRESENTATION('',(#27139),#259219);
#259390=PRODUCT_DEFINITION_CONTEXT('part definition',#259455,'design');
#259407=PRODUCT_DEFINITION('Journal thrust washer',
'Journal thrust washer',#259428,#259390);
#259428=PRODUCT_DEFINITION_FORMATION('',$,#259473);
#259455=APPLICATION_CONTEXT(
'Core Data for Automotive Mechanical Design Process');
#259456=PRODUCT_CONTEXT('part definition',#259455,'mechanical');
#259473=PRODUCT('Journal thrust washer','Journal thrust washer',$,(#259456));
#259485=PRESENTATION_STYLE_ASSIGNMENT((#259500));
#259500=SURFACE_STYLE_USAGE(.BOTH.,#259515);
#259515=SURFACE_SIDE_STYLE('',(#259530));
#259530=SURFACE_STYLE_FILL_AREA(#259545);
#259545=FILL_AREA_STYLE('Bearing light gray',(#259560));
#259560=FILL_AREA_STYLE_COLOUR('Bearing light gray',#259575);
#259575=COLOUR_RGB('Bearing light gray',0.725490196078431,0.752941176470588,
0.792156862745098);
ENDSEC;
END-ISO-10303-21;
